ISO-10303-21;
HEADER;
/* Generated by software containing ST-Developer
 * from STEP Tools, Inc. (www.steptools.com) 
 */

FILE_DESCRIPTION(
/* description */ ('Located fixture plate with toggle clamp'),
/* implementation_level */ '2;1');

FILE_NAME(
/* name */ 'Hex Nut - M8.step',
/* time_stamp */ '2026-10-27T21:36:12-07:00',
/* author */ (''),
/* organization */ (''),
/* preprocessor_version */ 'ST-DEVELOPER v20.2',
/* originating_system */ 'Autodesk Translation Framework v15.17.0.0',
/* authorisation */ '');

FILE_SCHEMA (('AUTOMOTIVE_DESIGN { 1 0 10303 214 3 1 1 }'));
ENDSEC;

DATA;
#10=MECHANICAL_DESIGN_GEOMETRIC_PRESENTATION_REPRESENTATION('',(#339),#9285);
#232=(
BOUNDED_CURVE()
B_SPLINE_CURVE(2,(#8890,#8891,#8892),.UNSPECIFIED.,.F.,.F.)
B_SPLINE_CURVE_WITH_KNOTS((3,3),(0.14973948338295,0.97160236658079),
 .UNSPECIFIED.)
CURVE()
GEOMETRIC_REPRESENTATION_ITEM()
RATIONAL_B_SPLINE_CURVE((1.07140024848292,1.23714644374248,1.07140024848292))
REPRESENTATION_ITEM('')
);
#233=(
BOUNDED_CURVE()
B_SPLINE_CURVE(2,(#8894,#8895,#8896),.UNSPECIFIED.,.F.,.F.)
B_SPLINE_CURVE_WITH_KNOTS((3,3),(0.14973948338295,0.971602366580789),
 .UNSPECIFIED.)
CURVE()
GEOMETRIC_REPRESENTATION_ITEM()
RATIONAL_B_SPLINE_CURVE((1.07140024848292,1.23714644374248,1.07140024848292))
REPRESENTATION_ITEM('')
);
#234=(
BOUNDED_CURVE()
B_SPLINE_CURVE(2,(#8901,#8902,#8903),.UNSPECIFIED.,.F.,.F.)
B_SPLINE_CURVE_WITH_KNOTS((3,3),(0.14973948338295,0.97160236658079),
 .UNSPECIFIED.)
CURVE()
GEOMETRIC_REPRESENTATION_ITEM()
RATIONAL_B_SPLINE_CURVE((1.07140024848292,1.23714644374248,1.07140024848292))
REPRESENTATION_ITEM('')
);
#235=(
BOUNDED_CURVE()
B_SPLINE_CURVE(2,(#8905,#8906,#8907),.UNSPECIFIED.,.F.,.F.)
B_SPLINE_CURVE_WITH_KNOTS((3,3),(0.14973948338295,0.97160236658079),
 .UNSPECIFIED.)
CURVE()
GEOMETRIC_REPRESENTATION_ITEM()
RATIONAL_B_SPLINE_CURVE((1.07140024848292,1.23714644374248,1.07140024848292))
REPRESENTATION_ITEM('')
);
#236=(
BOUNDED_CURVE()
B_SPLINE_CURVE(2,(#8909,#8910,#8911),.UNSPECIFIED.,.F.,.F.)
B_SPLINE_CURVE_WITH_KNOTS((3,3),(0.14973948338295,0.971602366580789),
 .UNSPECIFIED.)
CURVE()
GEOMETRIC_REPRESENTATION_ITEM()
RATIONAL_B_SPLINE_CURVE((1.07140024848292,1.23714644374248,1.07140024848292))
REPRESENTATION_ITEM('')
);
#237=(
BOUNDED_CURVE()
B_SPLINE_CURVE(2,(#8912,#8913,#8914),.UNSPECIFIED.,.F.,.F.)
B_SPLINE_CURVE_WITH_KNOTS((3,3),(0.14973948338295,0.97160236658079),
 .UNSPECIFIED.)
CURVE()
GEOMETRIC_REPRESENTATION_ITEM()
RATIONAL_B_SPLINE_CURVE((1.07140024848292,1.23714644374248,1.07140024848292))
REPRESENTATION_ITEM('')
);
#238=(
BOUNDED_CURVE()
B_SPLINE_CURVE(2,(#8921,#8922,#8923),.UNSPECIFIED.,.F.,.F.)
B_SPLINE_CURVE_WITH_KNOTS((3,3),(0.14973948338295,0.97160236658079),
 .UNSPECIFIED.)
CURVE()
GEOMETRIC_REPRESENTATION_ITEM()
RATIONAL_B_SPLINE_CURVE((1.07140024848292,1.23714644374248,1.07140024848292))
REPRESENTATION_ITEM('')
);
#239=(
BOUNDED_CURVE()
B_SPLINE_CURVE(2,(#8925,#8926,#8927),.UNSPECIFIED.,.F.,.F.)
B_SPLINE_CURVE_WITH_KNOTS((3,3),(0.14973948338295,0.97160236658079),
 .UNSPECIFIED.)
CURVE()
GEOMETRIC_REPRESENTATION_ITEM()
RATIONAL_B_SPLINE_CURVE((1.07140024848292,1.23714644374248,1.07140024848292))
REPRESENTATION_ITEM('')
);
#240=(
BOUNDED_CURVE()
B_SPLINE_CURVE(2,(#8929,#8930,#8931),.UNSPECIFIED.,.F.,.F.)
B_SPLINE_CURVE_WITH_KNOTS((3,3),(0.14973948338295,0.971602366580789),
 .UNSPECIFIED.)
CURVE()
GEOMETRIC_REPRESENTATION_ITEM()
RATIONAL_B_SPLINE_CURVE((1.07140024848292,1.23714644374248,1.07140024848292))
REPRESENTATION_ITEM('')
);
#241=(
BOUNDED_CURVE()
B_SPLINE_CURVE(2,(#8933,#8934,#8935),.UNSPECIFIED.,.F.,.F.)
B_SPLINE_CURVE_WITH_KNOTS((3,3),(0.14973948338295,0.97160236658079),
 .UNSPECIFIED.)
CURVE()
GEOMETRIC_REPRESENTATION_ITEM()
RATIONAL_B_SPLINE_CURVE((1.07140024848292,1.23714644374248,1.07140024848292))
REPRESENTATION_ITEM('')
);
#242=(
BOUNDED_CURVE()
B_SPLINE_CURVE(2,(#8937,#8938,#8939),.UNSPECIFIED.,.F.,.F.)
B_SPLINE_CURVE_WITH_KNOTS((3,3),(0.14973948338295,0.97160236658079),
 .UNSPECIFIED.)
CURVE()
GEOMETRIC_REPRESENTATION_ITEM()
RATIONAL_B_SPLINE_CURVE((1.07140024848292,1.23714644374248,1.07140024848292))
REPRESENTATION_ITEM('')
);
#243=(
BOUNDED_CURVE()
B_SPLINE_CURVE(2,(#8940,#8941,#8942),.UNSPECIFIED.,.F.,.F.)
B_SPLINE_CURVE_WITH_KNOTS((3,3),(0.14973948338295,0.971602366580789),
 .UNSPECIFIED.)
CURVE()
GEOMETRIC_REPRESENTATION_ITEM()
RATIONAL_B_SPLINE_CURVE((1.07140024848292,1.23714644374248,1.07140024848292))
REPRESENTATION_ITEM('')
);
#269=CONICAL_SURFACE('',#5919,0.734027674973257,1.0471975511966);
#270=CONICAL_SURFACE('',#5921,0.734027674973257,1.0471975511966);
#291=SHAPE_REPRESENTATION_RELATIONSHIP('SRR','None',#9417,#315);
#315=ADVANCED_BREP_SHAPE_REPRESENTATION('',(#360),#9279);
#339=STYLED_ITEM('',(#9619),#360);
#360=MANIFOLD_SOLID_BREP('Body1',#5190);
#477=FACE_BOUND('',#1349,.T.);
#478=FACE_BOUND('',#1351,.T.);
#653=PLANE('',#5923);
#654=PLANE('',#5924);
#655=PLANE('',#5925);
#656=PLANE('',#5929);
#657=PLANE('',#5930);
#658=PLANE('',#5931);
#659=PLANE('',#5932);
#660=PLANE('',#5933);
#933=FACE_OUTER_BOUND('',#1339,.T.);
#934=FACE_OUTER_BOUND('',#1340,.T.);
#935=FACE_OUTER_BOUND('',#1341,.T.);
#936=FACE_OUTER_BOUND('',#1342,.T.);
#937=FACE_OUTER_BOUND('',#1343,.T.);
#938=FACE_OUTER_BOUND('',#1344,.T.);
#939=FACE_OUTER_BOUND('',#1345,.T.);
#940=FACE_OUTER_BOUND('',#1346,.T.);
#941=FACE_OUTER_BOUND('',#1347,.T.);
#942=FACE_OUTER_BOUND('',#1348,.T.);
#943=FACE_OUTER_BOUND('',#1350,.T.);
#1339=EDGE_LOOP('',(#4656,#4657,#4658,#4659,#4660,#4661,#4662,#4663,#4664));
#1340=EDGE_LOOP('',(#4665,#4666,#4667,#4668,#4669,#4670,#4671,#4672,#4673));
#1341=EDGE_LOOP('',(#4674,#4675,#4676,#4677));
#1342=EDGE_LOOP('',(#4678,#4679,#4680,#4681));
#1343=EDGE_LOOP('',(#4682,#4683,#4684,#4685));
#1344=EDGE_LOOP('',(#4686,#4687,#4688,#4689));
#1345=EDGE_LOOP('',(#4690,#4691,#4692,#4693));
#1346=EDGE_LOOP('',(#4694,#4695,#4696,#4697));
#1347=EDGE_LOOP('',(#4698,#4699,#4700,#4701));
#1348=EDGE_LOOP('',(#4702));
#1349=EDGE_LOOP('',(#4703));
#1350=EDGE_LOOP('',(#4704));
#1351=EDGE_LOOP('',(#4705));
#1556=CIRCLE('',#5920,0.6175);
#1557=CIRCLE('',#5922,0.6175);
#1558=CIRCLE('',#5927,0.338975);
#1559=CIRCLE('',#5928,0.338975);
#1966=LINE('',#8898,#2376);
#1967=LINE('',#8919,#2377);
#1968=LINE('',#8944,#2378);
#1969=LINE('',#8945,#2379);
#1970=LINE('',#8947,#2380);
#1971=LINE('',#8949,#2381);
#1972=LINE('',#8954,#2382);
#1973=LINE('',#8957,#2383);
#1974=LINE('',#8959,#2384);
#2376=VECTOR('',#7332,0.734027674973257);
#2377=VECTOR('',#7339,0.734027674973257);
#2378=VECTOR('',#7342,1.);
#2379=VECTOR('',#7343,1.);
#2380=VECTOR('',#7346,1.);
#2381=VECTOR('',#7349,1.);
#2382=VECTOR('',#7354,0.4);
#2383=VECTOR('',#7359,1.);
#2384=VECTOR('',#7362,1.);
#2786=VERTEX_POINT('',#8888);
#2787=VERTEX_POINT('',#8889);
#2788=VERTEX_POINT('',#8893);
#2789=VERTEX_POINT('',#8897);
#2790=VERTEX_POINT('',#8900);
#2791=VERTEX_POINT('',#8904);
#2792=VERTEX_POINT('',#8908);
#2793=VERTEX_POINT('',#8916);
#2794=VERTEX_POINT('',#8918);
#2795=VERTEX_POINT('',#8920);
#2796=VERTEX_POINT('',#8924);
#2797=VERTEX_POINT('',#8928);
#2798=VERTEX_POINT('',#8932);
#2799=VERTEX_POINT('',#8936);
#2800=VERTEX_POINT('',#8951);
#2801=VERTEX_POINT('',#8953);
#3416=EDGE_CURVE('',#2786,#2787,#232,.T.);
#3417=EDGE_CURVE('',#2788,#2786,#233,.T.);
#3418=EDGE_CURVE('',#2788,#2789,#1966,.T.);
#3419=EDGE_CURVE('',#2789,#2789,#1556,.T.);
#3420=EDGE_CURVE('',#2790,#2788,#234,.T.);
#3421=EDGE_CURVE('',#2791,#2790,#235,.T.);
#3422=EDGE_CURVE('',#2792,#2791,#236,.T.);
#3423=EDGE_CURVE('',#2787,#2792,#237,.T.);
#3424=EDGE_CURVE('',#2793,#2793,#1557,.T.);
#3425=EDGE_CURVE('',#2793,#2794,#1967,.T.);
#3426=EDGE_CURVE('',#2795,#2794,#238,.T.);
#3427=EDGE_CURVE('',#2796,#2795,#239,.T.);
#3428=EDGE_CURVE('',#2797,#2796,#240,.T.);
#3429=EDGE_CURVE('',#2798,#2797,#241,.T.);
#3430=EDGE_CURVE('',#2799,#2798,#242,.T.);
#3431=EDGE_CURVE('',#2794,#2799,#243,.T.);
#3432=EDGE_CURVE('',#2790,#2799,#1968,.T.);
#3433=EDGE_CURVE('',#2791,#2798,#1969,.T.);
#3434=EDGE_CURVE('',#2788,#2794,#1970,.T.);
#3435=EDGE_CURVE('',#2786,#2795,#1971,.T.);
#3436=EDGE_CURVE('',#2800,#2800,#1558,.F.);
#3437=EDGE_CURVE('',#2800,#2801,#1972,.T.);
#3438=EDGE_CURVE('',#2801,#2801,#1559,.F.);
#3439=EDGE_CURVE('',#2787,#2796,#1973,.T.);
#3440=EDGE_CURVE('',#2792,#2797,#1974,.T.);
#4656=ORIENTED_EDGE('',*,*,#3416,.F.);
#4657=ORIENTED_EDGE('',*,*,#3417,.F.);
#4658=ORIENTED_EDGE('',*,*,#3418,.T.);
#4659=ORIENTED_EDGE('',*,*,#3419,.F.);
#4660=ORIENTED_EDGE('',*,*,#3418,.F.);
#4661=ORIENTED_EDGE('',*,*,#3420,.F.);
#4662=ORIENTED_EDGE('',*,*,#3421,.F.);
#4663=ORIENTED_EDGE('',*,*,#3422,.F.);
#4664=ORIENTED_EDGE('',*,*,#3423,.F.);
#4665=ORIENTED_EDGE('',*,*,#3424,.F.);
#4666=ORIENTED_EDGE('',*,*,#3425,.T.);
#4667=ORIENTED_EDGE('',*,*,#3426,.F.);
#4668=ORIENTED_EDGE('',*,*,#3427,.F.);
#4669=ORIENTED_EDGE('',*,*,#3428,.F.);
#4670=ORIENTED_EDGE('',*,*,#3429,.F.);
#4671=ORIENTED_EDGE('',*,*,#3430,.F.);
#4672=ORIENTED_EDGE('',*,*,#3431,.F.);
#4673=ORIENTED_EDGE('',*,*,#3425,.F.);
#4674=ORIENTED_EDGE('',*,*,#3421,.T.);
#4675=ORIENTED_EDGE('',*,*,#3432,.T.);
#4676=ORIENTED_EDGE('',*,*,#3430,.T.);
#4677=ORIENTED_EDGE('',*,*,#3433,.F.);
#4678=ORIENTED_EDGE('',*,*,#3420,.T.);
#4679=ORIENTED_EDGE('',*,*,#3434,.T.);
#4680=ORIENTED_EDGE('',*,*,#3431,.T.);
#4681=ORIENTED_EDGE('',*,*,#3432,.F.);
#4682=ORIENTED_EDGE('',*,*,#3417,.T.);
#4683=ORIENTED_EDGE('',*,*,#3435,.T.);
#4684=ORIENTED_EDGE('',*,*,#3426,.T.);
#4685=ORIENTED_EDGE('',*,*,#3434,.F.);
#4686=ORIENTED_EDGE('',*,*,#3436,.F.);
#4687=ORIENTED_EDGE('',*,*,#3437,.T.);
#4688=ORIENTED_EDGE('',*,*,#3438,.T.);
#4689=ORIENTED_EDGE('',*,*,#3437,.F.);
#4690=ORIENTED_EDGE('',*,*,#3416,.T.);
#4691=ORIENTED_EDGE('',*,*,#3439,.T.);
#4692=ORIENTED_EDGE('',*,*,#3427,.T.);
#4693=ORIENTED_EDGE('',*,*,#3435,.F.);
#4694=ORIENTED_EDGE('',*,*,#3422,.T.);
#4695=ORIENTED_EDGE('',*,*,#3433,.T.);
#4696=ORIENTED_EDGE('',*,*,#3429,.T.);
#4697=ORIENTED_EDGE('',*,*,#3440,.F.);
#4698=ORIENTED_EDGE('',*,*,#3423,.T.);
#4699=ORIENTED_EDGE('',*,*,#3440,.T.);
#4700=ORIENTED_EDGE('',*,*,#3428,.T.);
#4701=ORIENTED_EDGE('',*,*,#3439,.F.);
#4702=ORIENTED_EDGE('',*,*,#3424,.T.);
#4703=ORIENTED_EDGE('',*,*,#3436,.T.);
#4704=ORIENTED_EDGE('',*,*,#3419,.T.);
#4705=ORIENTED_EDGE('',*,*,#3438,.F.);
#4864=CYLINDRICAL_SURFACE('',#5926,0.338975);
#5134=ADVANCED_FACE('',(#933),#269,.T.);
#5135=ADVANCED_FACE('',(#934),#270,.T.);
#5136=ADVANCED_FACE('',(#935),#653,.T.);
#5137=ADVANCED_FACE('',(#936),#654,.T.);
#5138=ADVANCED_FACE('',(#937),#655,.T.);
#5139=ADVANCED_FACE('',(#938),#4864,.F.);
#5140=ADVANCED_FACE('',(#939),#656,.T.);
#5141=ADVANCED_FACE('',(#940),#657,.T.);
#5142=ADVANCED_FACE('',(#941),#658,.T.);
#5143=ADVANCED_FACE('',(#942,#477),#659,.T.);
#5144=ADVANCED_FACE('',(#943,#478),#660,.F.);
#5190=CLOSED_SHELL('',(#5134,#5135,#5136,#5137,#5138,#5139,#5140,#5141,
#5142,#5143,#5144));
#5918=AXIS2_PLACEMENT_3D('',#8886,#7328,#7329);
#5919=AXIS2_PLACEMENT_3D('',#8887,#7330,#7331);
#5920=AXIS2_PLACEMENT_3D('',#8899,#7333,#7334);
#5921=AXIS2_PLACEMENT_3D('',#8915,#7335,#7336);
#5922=AXIS2_PLACEMENT_3D('',#8917,#7337,#7338);
#5923=AXIS2_PLACEMENT_3D('',#8943,#7340,#7341);
#5924=AXIS2_PLACEMENT_3D('',#8946,#7344,#7345);
#5925=AXIS2_PLACEMENT_3D('',#8948,#7347,#7348);
#5926=AXIS2_PLACEMENT_3D('',#8950,#7350,#7351);
#5927=AXIS2_PLACEMENT_3D('',#8952,#7352,#7353);
#5928=AXIS2_PLACEMENT_3D('',#8955,#7355,#7356);
#5929=AXIS2_PLACEMENT_3D('',#8956,#7357,#7358);
#5930=AXIS2_PLACEMENT_3D('',#8958,#7360,#7361);
#5931=AXIS2_PLACEMENT_3D('',#8960,#7363,#7364);
#5932=AXIS2_PLACEMENT_3D('',#8961,#7365,#7366);
#5933=AXIS2_PLACEMENT_3D('',#8962,#7367,#7368);
#7328=DIRECTION('axis',(0.,0.,1.));
#7329=DIRECTION('refdir',(1.,0.,0.));
#7330=DIRECTION('center_axis',(0.,1.,0.));
#7331=DIRECTION('ref_axis',(1.,0.,0.));
#7332=DIRECTION('',(0.866025403784439,-0.5,1.06057523872491E-16));
#7333=DIRECTION('center_axis',(0.,-1.,0.));
#7334=DIRECTION('ref_axis',(1.,0.,0.));
#7335=DIRECTION('center_axis',(0.,-1.,0.));
#7336=DIRECTION('ref_axis',(1.,0.,0.));
#7337=DIRECTION('center_axis',(0.,1.,0.));
#7338=DIRECTION('ref_axis',(1.,0.,0.));
#7339=DIRECTION('',(-0.866025403784439,-0.5,-1.06057523872491E-16));
#7340=DIRECTION('center_axis',(1.4792020664489E-16,0.,-1.));
#7341=DIRECTION('ref_axis',(-1.,0.,-1.4792020664489E-16));
#7342=DIRECTION('',(0.,1.,0.));
#7343=DIRECTION('',(0.,1.,0.));
#7344=DIRECTION('center_axis',(-0.866025403784439,0.,-0.5));
#7345=DIRECTION('ref_axis',(-0.5,0.,0.866025403784439));
#7346=DIRECTION('',(0.,1.,0.));
#7347=DIRECTION('center_axis',(-0.866025403784439,0.,0.5));
#7348=DIRECTION('ref_axis',(0.5,0.,0.866025403784439));
#7349=DIRECTION('',(0.,1.,0.));
#7350=DIRECTION('center_axis',(0.,1.,0.));
#7351=DIRECTION('ref_axis',(1.,0.,0.));
#7352=DIRECTION('center_axis',(0.,1.,0.));
#7353=DIRECTION('ref_axis',(1.,0.,0.));
#7354=DIRECTION('',(0.,-1.,0.));
#7355=DIRECTION('center_axis',(0.,1.,0.));
#7356=DIRECTION('ref_axis',(1.,0.,0.));
#7357=DIRECTION('center_axis',(-2.95840413289779E-16,0.,1.));
#7358=DIRECTION('ref_axis',(1.,0.,2.95840413289779E-16));
#7359=DIRECTION('',(0.,1.,0.));
#7360=DIRECTION('center_axis',(0.866025403784439,0.,-0.5));
#7361=DIRECTION('ref_axis',(-0.5,0.,-0.866025403784439));
#7362=DIRECTION('',(0.,1.,0.));
#7363=DIRECTION('center_axis',(0.866025403784439,0.,0.5));
#7364=DIRECTION('ref_axis',(0.5,0.,-0.866025403784439));
#7365=DIRECTION('center_axis',(0.,1.,0.));
#7366=DIRECTION('ref_axis',(1.,0.,0.));
#7367=DIRECTION('center_axis',(0.,1.,0.));
#7368=DIRECTION('ref_axis',(1.,0.,0.));
#8886=CARTESIAN_POINT('',(0.,0.,0.));
#8887=CARTESIAN_POINT('Origin',(0.,0.067277284513851,0.));
#8888=CARTESIAN_POINT('',(-0.375277674973257,0.0768195421087395,0.65));
#8889=CARTESIAN_POINT('',(0.375277674973257,0.0768195421087395,0.65));
#8890=CARTESIAN_POINT('Ctrl Pts',(-0.375277674973257,0.0768195421087395,
0.65));
#8891=CARTESIAN_POINT('Ctrl Pts',(1.66533453693773E-13,-0.0315137912242439,
0.65));
#8892=CARTESIAN_POINT('Ctrl Pts',(0.375277674973257,0.0768195421087394,
0.65));
#8893=CARTESIAN_POINT('',(-0.750555349946514,0.0768195421087394,-9.19165206894919E-17));
#8894=CARTESIAN_POINT('Ctrl Pts',(-0.750555349946514,0.0768195421087394,
-9.19165206894919E-17));
#8895=CARTESIAN_POINT('Ctrl Pts',(-0.562916512459802,-0.0315137912242434,
0.325000000000144));
#8896=CARTESIAN_POINT('Ctrl Pts',(-0.375277674973257,0.0768195421087395,
0.65));
#8897=CARTESIAN_POINT('',(-0.6175,-2.77555756156289E-17,-7.5621939847349E-17));
#8898=CARTESIAN_POINT('',(-0.734027674973257,0.067277284513851,-8.98924642641573E-17));
#8899=CARTESIAN_POINT('Origin',(0.,0.,0.));
#8900=CARTESIAN_POINT('',(-0.375277674973257,0.0768195421087395,-0.65));
#8901=CARTESIAN_POINT('Ctrl Pts',(-0.375277674973257,0.0768195421087395,
-0.65));
#8902=CARTESIAN_POINT('Ctrl Pts',(-0.562916512459968,-0.0315137912242437,
-0.324999999999856));
#8903=CARTESIAN_POINT('Ctrl Pts',(-0.750555349946514,0.0768195421087395,
-9.19165206894919E-17));
#8904=CARTESIAN_POINT('',(0.375277674973257,0.0768195421087395,-0.65));
#8905=CARTESIAN_POINT('Ctrl Pts',(0.375277674973257,0.0768195421087395,
-0.65));
#8906=CARTESIAN_POINT('Ctrl Pts',(-1.66144875635155E-13,-0.0315137912242437,
-0.65));
#8907=CARTESIAN_POINT('Ctrl Pts',(-0.375277674973257,0.0768195421087395,
-0.65));
#8908=CARTESIAN_POINT('',(0.750555349946514,0.0768195421087394,0.));
#8909=CARTESIAN_POINT('Ctrl Pts',(0.750555349946514,0.0768195421087394,
0.));
#8910=CARTESIAN_POINT('Ctrl Pts',(0.562916512459802,-0.0315137912242436,
-0.325000000000144));
#8911=CARTESIAN_POINT('Ctrl Pts',(0.375277674973257,0.0768195421087395,
-0.65));
#8912=CARTESIAN_POINT('Ctrl Pts',(0.375277674973257,0.0768195421087394,
0.65));
#8913=CARTESIAN_POINT('Ctrl Pts',(0.562916512459968,-0.0315137912242439,
0.324999999999856));
#8914=CARTESIAN_POINT('Ctrl Pts',(0.750555349946514,0.0768195421087394,
0.));
#8915=CARTESIAN_POINT('Origin',(0.,0.612722715486149,0.));
#8916=CARTESIAN_POINT('',(-0.6175,0.68,-7.5621939847349E-17));
#8917=CARTESIAN_POINT('Origin',(0.,0.68,0.));
#8918=CARTESIAN_POINT('',(-0.750555349946514,0.603180457891261,-9.19165206894919E-17));
#8919=CARTESIAN_POINT('',(-0.734027674973257,0.612722715486149,-8.98924642641573E-17));
#8920=CARTESIAN_POINT('',(-0.375277674973257,0.603180457891261,0.65));
#8921=CARTESIAN_POINT('Ctrl Pts',(-0.375277674973257,0.603180457891261,
0.65));
#8922=CARTESIAN_POINT('Ctrl Pts',(-0.562916512459968,0.711513791224243,
0.324999999999856));
#8923=CARTESIAN_POINT('Ctrl Pts',(-0.750555349946514,0.603180457891261,
-9.19165206894919E-17));
#8924=CARTESIAN_POINT('',(0.375277674973257,0.603180457891261,0.65));
#8925=CARTESIAN_POINT('Ctrl Pts',(0.375277674973257,0.603180457891261,0.65));
#8926=CARTESIAN_POINT('Ctrl Pts',(-1.66755498298699E-13,0.711513791224244,
0.65));
#8927=CARTESIAN_POINT('Ctrl Pts',(-0.375277674973257,0.603180457891261,
0.65));
#8928=CARTESIAN_POINT('',(0.750555349946514,0.603180457891261,0.));
#8929=CARTESIAN_POINT('Ctrl Pts',(0.750555349946514,0.603180457891261,0.));
#8930=CARTESIAN_POINT('Ctrl Pts',(0.562916512459802,0.711513791224244,0.325000000000144));
#8931=CARTESIAN_POINT('Ctrl Pts',(0.375277674973257,0.603180457891261,0.65));
#8932=CARTESIAN_POINT('',(0.375277674973257,0.603180457891261,-0.65));
#8933=CARTESIAN_POINT('Ctrl Pts',(0.375277674973257,0.603180457891261,-0.65));
#8934=CARTESIAN_POINT('Ctrl Pts',(0.562916512459969,0.711513791224244,-0.324999999999856));
#8935=CARTESIAN_POINT('Ctrl Pts',(0.750555349946514,0.603180457891261,0.));
#8936=CARTESIAN_POINT('',(-0.375277674973257,0.603180457891261,-0.65));
#8937=CARTESIAN_POINT('Ctrl Pts',(-0.375277674973257,0.603180457891261,
-0.65));
#8938=CARTESIAN_POINT('Ctrl Pts',(1.66422431391311E-13,0.711513791224244,
-0.65));
#8939=CARTESIAN_POINT('Ctrl Pts',(0.375277674973257,0.603180457891261,-0.65));
#8940=CARTESIAN_POINT('Ctrl Pts',(-0.750555349946514,0.603180457891261,
-9.19165206894919E-17));
#8941=CARTESIAN_POINT('Ctrl Pts',(-0.562916512459802,0.711513791224244,
-0.325000000000144));
#8942=CARTESIAN_POINT('Ctrl Pts',(-0.375277674973257,0.603180457891261,
-0.65));
#8943=CARTESIAN_POINT('Origin',(0.375277674973257,0.,-0.65));
#8944=CARTESIAN_POINT('',(-0.375277674973257,0.,-0.65));
#8945=CARTESIAN_POINT('',(0.375277674973257,0.,-0.65));
#8946=CARTESIAN_POINT('Origin',(-0.375277674973257,0.,-0.65));
#8947=CARTESIAN_POINT('',(-0.750555349946514,0.,-9.19165206894919E-17));
#8948=CARTESIAN_POINT('Origin',(-0.750555349946514,0.,-9.19165206894919E-17));
#8949=CARTESIAN_POINT('',(-0.375277674973257,0.,0.65));
#8950=CARTESIAN_POINT('Origin',(0.,0.,0.));
#8951=CARTESIAN_POINT('',(-0.338975,0.68,4.15124648740974E-17));
#8952=CARTESIAN_POINT('Origin',(0.,0.68,0.));
#8953=CARTESIAN_POINT('',(-0.338975,0.,4.15124648740974E-17));
#8954=CARTESIAN_POINT('',(-0.338975,0.,4.15124648740974E-17));
#8955=CARTESIAN_POINT('Origin',(0.,0.,0.));
#8956=CARTESIAN_POINT('Origin',(-0.375277674973257,0.,0.65));
#8957=CARTESIAN_POINT('',(0.375277674973257,0.,0.65));
#8958=CARTESIAN_POINT('Origin',(0.750555349946514,0.,0.));
#8959=CARTESIAN_POINT('',(0.750555349946514,0.,0.));
#8960=CARTESIAN_POINT('Origin',(0.375277674973257,0.,0.65));
#8961=CARTESIAN_POINT('Origin',(0.,0.68,-1.11022302462516E-16));
#8962=CARTESIAN_POINT('Origin',(0.,0.,-1.11022302462516E-16));
#9249=UNCERTAINTY_MEASURE_WITH_UNIT(LENGTH_MEASURE(0.001),#9286,
'DISTANCE_ACCURACY_VALUE',
'Maximum model space distance between geometric entities at asserted c
onnectivities');
#9255=UNCERTAINTY_MEASURE_WITH_UNIT(LENGTH_MEASURE(0.001),#9286,
'DISTANCE_ACCURACY_VALUE',
'Maximum model space distance between geometric entities at asserted c
onnectivities');
#9279=(
GEOMETRIC_REPRESENTATION_CONTEXT(3)
GLOBAL_UNCERTAINTY_ASSIGNED_CONTEXT((#9249))
GLOBAL_UNIT_ASSIGNED_CONTEXT((#9286,#9288,#9289))
REPRESENTATION_CONTEXT('','3D')
);
#9285=(
GEOMETRIC_REPRESENTATION_CONTEXT(3)
GLOBAL_UNCERTAINTY_ASSIGNED_CONTEXT((#9255))
GLOBAL_UNIT_ASSIGNED_CONTEXT((#9286,#9288,#9289))
REPRESENTATION_CONTEXT('','3D')
);
#9286=(
LENGTH_UNIT()
NAMED_UNIT(*)
SI_UNIT(.CENTI.,.METRE.)
);
#9288=(
NAMED_UNIT(*)
PLANE_ANGLE_UNIT()
SI_UNIT($,.RADIAN.)
);
#9289=(
NAMED_UNIT(*)
SI_UNIT($,.STERADIAN.)
SOLID_ANGLE_UNIT()
);
#9313=SHAPE_DEFINITION_REPRESENTATION(#9343,#9417);
#9343=PRODUCT_DEFINITION_SHAPE('',$,#9447);
#9417=SHAPE_REPRESENTATION('',(#5918),#9279);
#9423=PRODUCT_DEFINITION_CONTEXT('part definition',#9512,'design');
#9447=PRODUCT_DEFINITION('Hex Nut - M8','Hex Nut - M8',#9476,#9423);
#9476=PRODUCT_DEFINITION_FORMATION('',$,#9537);
#9512=APPLICATION_CONTEXT(
'Core Data for Automotive Mechanical Design Process');
#9513=PRODUCT_CONTEXT('part definition',#9512,'mechanical');
#9537=PRODUCT('Hex Nut - M8','Hex Nut - M8','Hex Nut - M8',(#9513));
#9613=COLOUR_RGB('Black',0.12,0.14,0.17);
#9614=FILL_AREA_STYLE_COLOUR('',#9613);
#9615=FILL_AREA_STYLE('',(#9614));
#9616=SURFACE_STYLE_FILL_AREA(#9615);
#9617=SURFACE_SIDE_STYLE('',(#9616));
#9618=SURFACE_STYLE_USAGE(.BOTH.,#9617);
#9619=PRESENTATION_STYLE_ASSIGNMENT((#9618));
ENDSEC;
END-ISO-10303-21;
